ISO-10303-21;
HEADER;
/* Generated by software containing ST-Developer
 * from STEP Tools, Inc. (www.steptools.com) 
 */

FILE_DESCRIPTION(
/* description */ ('Lifting hook block with sheave'),
/* implementation_level */ '2;1');

FILE_NAME(
/* name */ 'M4x10 Cap Screw.step',
/* time_stamp */ '2026-10-28T03:23:54-07:00',
/* author */ (''),
/* organization */ (''),
/* preprocessor_version */ 'ST-DEVELOPER v20.2',
/* originating_system */ 'Autodesk Translation Framework v15.17.0.0',
/* authorisation */ '');

FILE_SCHEMA (('AUTOMOTIVE_DESIGN { 1 0 10303 214 3 1 1 }'));
ENDSEC;

DATA;
#10=MECHANICAL_DESIGN_GEOMETRIC_PRESENTATION_REPRESENTATION('',(#384),#9391);
#282=CONICAL_SURFACE('',#5829,0.325,0.785398163397448);
#283=CONICAL_SURFACE('',#5833,0.335,0.785398163397448);
#284=CONICAL_SURFACE('',#5837,0.21,0.463647609000806);
#287=ORIENTED_CLOSED_SHELL('',*,#4922,.F.);
#290=BREP_WITH_VOIDS('Body1',#4923,(#287));
#316=SHAPE_REPRESENTATION_RELATIONSHIP('SRR','None',#9549,#346);
#346=ADVANCED_BREP_SHAPE_REPRESENTATION('',(#290),#9384);
#384=STYLED_ITEM('',(#9766),#290);
#642=LINE('',#9072,#930);
#643=LINE('',#9074,#931);
#644=LINE('',#9076,#932);
#645=LINE('',#9077,#933);
#646=LINE('',#9080,#934);
#647=LINE('',#9082,#935);
#648=LINE('',#9083,#936);
#649=LINE('',#9086,#937);
#650=LINE('',#9088,#938);
#651=LINE('',#9089,#939);
#652=LINE('',#9092,#940);
#653=LINE('',#9094,#941);
#654=LINE('',#9095,#942);
#655=LINE('',#9098,#943);
#656=LINE('',#9100,#944);
#657=LINE('',#9101,#945);
#658=LINE('',#9103,#946);
#659=LINE('',#9104,#947);
#660=LINE('',#9116,#948);
#661=LINE('',#9120,#949);
#662=LINE('',#9124,#950);
#663=LINE('',#9131,#951);
#664=LINE('',#9133,#952);
#930=VECTOR('',#7265,1.);
#931=VECTOR('',#7266,1.);
#932=VECTOR('',#7267,1.);
#933=VECTOR('',#7268,1.);
#934=VECTOR('',#7271,1.);
#935=VECTOR('',#7272,1.);
#936=VECTOR('',#7273,1.);
#937=VECTOR('',#7276,1.);
#938=VECTOR('',#7277,1.);
#939=VECTOR('',#7278,1.);
#940=VECTOR('',#7281,1.);
#941=VECTOR('',#7282,1.);
#942=VECTOR('',#7283,1.);
#943=VECTOR('',#7286,1.);
#944=VECTOR('',#7287,1.);
#945=VECTOR('',#7288,1.);
#946=VECTOR('',#7291,1.);
#947=VECTOR('',#7292,1.);
#948=VECTOR('',#7309,0.325);
#949=VECTOR('',#7314,0.35);
#950=VECTOR('',#7319,0.335);
#951=VECTOR('',#7328,0.21);
#952=VECTOR('',#7331,0.2);
#1093=CYLINDRICAL_SURFACE('',#5831,0.35);
#1094=CYLINDRICAL_SURFACE('',#5839,0.1954);
#1211=FACE_BOUND('',#1867,.T.);
#1460=FACE_OUTER_BOUND('',#1853,.T.);
#1461=FACE_OUTER_BOUND('',#1854,.T.);
#1462=FACE_OUTER_BOUND('',#1855,.T.);
#1463=FACE_OUTER_BOUND('',#1856,.T.);
#1464=FACE_OUTER_BOUND('',#1857,.T.);
#1465=FACE_OUTER_BOUND('',#1858,.T.);
#1466=FACE_OUTER_BOUND('',#1859,.T.);
#1467=FACE_OUTER_BOUND('',#1860,.T.);
#1468=FACE_OUTER_BOUND('',#1861,.T.);
#1469=FACE_OUTER_BOUND('',#1862,.T.);
#1470=FACE_OUTER_BOUND('',#1863,.T.);
#1471=FACE_OUTER_BOUND('',#1864,.T.);
#1472=FACE_OUTER_BOUND('',#1865,.T.);
#1473=FACE_OUTER_BOUND('',#1866,.T.);
#1474=FACE_OUTER_BOUND('',#1868,.T.);
#1475=FACE_OUTER_BOUND('',#1869,.T.);
#1853=EDGE_LOOP('',(#4246,#4247,#4248,#4249));
#1854=EDGE_LOOP('',(#4250,#4251,#4252,#4253));
#1855=EDGE_LOOP('',(#4254,#4255,#4256,#4257));
#1856=EDGE_LOOP('',(#4258,#4259,#4260,#4261));
#1857=EDGE_LOOP('',(#4262,#4263,#4264,#4265));
#1858=EDGE_LOOP('',(#4266,#4267,#4268,#4269));
#1859=EDGE_LOOP('',(#4270,#4271,#4272,#4273,#4274,#4275));
#1860=EDGE_LOOP('',(#4276,#4277,#4278,#4279,#4280,#4281));
#1861=EDGE_LOOP('',(#4282));
#1862=EDGE_LOOP('',(#4283));
#1863=EDGE_LOOP('',(#4284,#4285,#4286,#4287));
#1864=EDGE_LOOP('',(#4288,#4289,#4290,#4291));
#1865=EDGE_LOOP('',(#4292,#4293,#4294,#4295));
#1866=EDGE_LOOP('',(#4296));
#1867=EDGE_LOOP('',(#4297));
#1868=EDGE_LOOP('',(#4298,#4299,#4300,#4301));
#1869=EDGE_LOOP('',(#4302,#4303,#4304,#4305));
#2175=CIRCLE('',#5826,0.1954);
#2176=CIRCLE('',#5828,0.3);
#2177=CIRCLE('',#5830,0.35);
#2178=CIRCLE('',#5832,0.35);
#2179=CIRCLE('',#5834,0.32);
#2180=CIRCLE('',#5836,0.22);
#2181=CIRCLE('',#5838,0.1954);
#2552=VERTEX_POINT('',#9070);
#2553=VERTEX_POINT('',#9071);
#2554=VERTEX_POINT('',#9073);
#2555=VERTEX_POINT('',#9075);
#2556=VERTEX_POINT('',#9079);
#2557=VERTEX_POINT('',#9081);
#2558=VERTEX_POINT('',#9085);
#2559=VERTEX_POINT('',#9087);
#2560=VERTEX_POINT('',#9091);
#2561=VERTEX_POINT('',#9093);
#2562=VERTEX_POINT('',#9097);
#2563=VERTEX_POINT('',#9099);
#2564=VERTEX_POINT('',#9108);
#2565=VERTEX_POINT('',#9111);
#2566=VERTEX_POINT('',#9114);
#2567=VERTEX_POINT('',#9118);
#2568=VERTEX_POINT('',#9122);
#2569=VERTEX_POINT('',#9126);
#2570=VERTEX_POINT('',#9129);
#3127=EDGE_CURVE('',#2552,#2553,#642,.T.);
#3128=EDGE_CURVE('',#2553,#2554,#643,.T.);
#3129=EDGE_CURVE('',#2554,#2555,#644,.T.);
#3130=EDGE_CURVE('',#2552,#2555,#645,.T.);
#3131=EDGE_CURVE('',#2553,#2556,#646,.T.);
#3132=EDGE_CURVE('',#2556,#2557,#647,.T.);
#3133=EDGE_CURVE('',#2557,#2554,#648,.T.);
#3134=EDGE_CURVE('',#2556,#2558,#649,.T.);
#3135=EDGE_CURVE('',#2558,#2559,#650,.T.);
#3136=EDGE_CURVE('',#2559,#2557,#651,.T.);
#3137=EDGE_CURVE('',#2558,#2560,#652,.T.);
#3138=EDGE_CURVE('',#2560,#2561,#653,.T.);
#3139=EDGE_CURVE('',#2561,#2559,#654,.T.);
#3140=EDGE_CURVE('',#2560,#2562,#655,.T.);
#3141=EDGE_CURVE('',#2562,#2563,#656,.T.);
#3142=EDGE_CURVE('',#2563,#2561,#657,.T.);
#3143=EDGE_CURVE('',#2562,#2552,#658,.T.);
#3144=EDGE_CURVE('',#2555,#2563,#659,.T.);
#3145=EDGE_CURVE('',#2564,#2564,#2175,.T.);
#3146=EDGE_CURVE('',#2565,#2565,#2176,.T.);
#3147=EDGE_CURVE('',#2566,#2566,#2177,.T.);
#3148=EDGE_CURVE('',#2566,#2565,#660,.T.);
#3149=EDGE_CURVE('',#2567,#2567,#2178,.T.);
#3150=EDGE_CURVE('',#2567,#2566,#661,.T.);
#3151=EDGE_CURVE('',#2568,#2568,#2179,.T.);
#3152=EDGE_CURVE('',#2568,#2567,#662,.T.);
#3153=EDGE_CURVE('',#2569,#2569,#2180,.T.);
#3154=EDGE_CURVE('',#2570,#2570,#2181,.F.);
#3155=EDGE_CURVE('',#2570,#2569,#663,.T.);
#3156=EDGE_CURVE('',#2564,#2570,#664,.T.);
#4246=ORIENTED_EDGE('',*,*,#3127,.T.);
#4247=ORIENTED_EDGE('',*,*,#3128,.T.);
#4248=ORIENTED_EDGE('',*,*,#3129,.T.);
#4249=ORIENTED_EDGE('',*,*,#3130,.F.);
#4250=ORIENTED_EDGE('',*,*,#3131,.T.);
#4251=ORIENTED_EDGE('',*,*,#3132,.T.);
#4252=ORIENTED_EDGE('',*,*,#3133,.T.);
#4253=ORIENTED_EDGE('',*,*,#3128,.F.);
#4254=ORIENTED_EDGE('',*,*,#3134,.T.);
#4255=ORIENTED_EDGE('',*,*,#3135,.T.);
#4256=ORIENTED_EDGE('',*,*,#3136,.T.);
#4257=ORIENTED_EDGE('',*,*,#3132,.F.);
#4258=ORIENTED_EDGE('',*,*,#3137,.T.);
#4259=ORIENTED_EDGE('',*,*,#3138,.T.);
#4260=ORIENTED_EDGE('',*,*,#3139,.T.);
#4261=ORIENTED_EDGE('',*,*,#3135,.F.);
#4262=ORIENTED_EDGE('',*,*,#3140,.T.);
#4263=ORIENTED_EDGE('',*,*,#3141,.T.);
#4264=ORIENTED_EDGE('',*,*,#3142,.T.);
#4265=ORIENTED_EDGE('',*,*,#3138,.F.);
#4266=ORIENTED_EDGE('',*,*,#3143,.T.);
#4267=ORIENTED_EDGE('',*,*,#3130,.T.);
#4268=ORIENTED_EDGE('',*,*,#3144,.T.);
#4269=ORIENTED_EDGE('',*,*,#3141,.F.);
#4270=ORIENTED_EDGE('',*,*,#3143,.F.);
#4271=ORIENTED_EDGE('',*,*,#3140,.F.);
#4272=ORIENTED_EDGE('',*,*,#3137,.F.);
#4273=ORIENTED_EDGE('',*,*,#3134,.F.);
#4274=ORIENTED_EDGE('',*,*,#3131,.F.);
#4275=ORIENTED_EDGE('',*,*,#3127,.F.);
#4276=ORIENTED_EDGE('',*,*,#3144,.F.);
#4277=ORIENTED_EDGE('',*,*,#3129,.F.);
#4278=ORIENTED_EDGE('',*,*,#3133,.F.);
#4279=ORIENTED_EDGE('',*,*,#3136,.F.);
#4280=ORIENTED_EDGE('',*,*,#3139,.F.);
#4281=ORIENTED_EDGE('',*,*,#3142,.F.);
#4282=ORIENTED_EDGE('',*,*,#3145,.F.);
#4283=ORIENTED_EDGE('',*,*,#3146,.F.);
#4284=ORIENTED_EDGE('',*,*,#3147,.F.);
#4285=ORIENTED_EDGE('',*,*,#3148,.T.);
#4286=ORIENTED_EDGE('',*,*,#3146,.T.);
#4287=ORIENTED_EDGE('',*,*,#3148,.F.);
#4288=ORIENTED_EDGE('',*,*,#3149,.F.);
#4289=ORIENTED_EDGE('',*,*,#3150,.T.);
#4290=ORIENTED_EDGE('',*,*,#3147,.T.);
#4291=ORIENTED_EDGE('',*,*,#3150,.F.);
#4292=ORIENTED_EDGE('',*,*,#3151,.F.);
#4293=ORIENTED_EDGE('',*,*,#3152,.T.);
#4294=ORIENTED_EDGE('',*,*,#3149,.T.);
#4295=ORIENTED_EDGE('',*,*,#3152,.F.);
#4296=ORIENTED_EDGE('',*,*,#3151,.T.);
#4297=ORIENTED_EDGE('',*,*,#3153,.F.);
#4298=ORIENTED_EDGE('',*,*,#3154,.F.);
#4299=ORIENTED_EDGE('',*,*,#3155,.T.);
#4300=ORIENTED_EDGE('',*,*,#3153,.T.);
#4301=ORIENTED_EDGE('',*,*,#3155,.F.);
#4302=ORIENTED_EDGE('',*,*,#3145,.T.);
#4303=ORIENTED_EDGE('',*,*,#3156,.T.);
#4304=ORIENTED_EDGE('',*,*,#3154,.T.);
#4305=ORIENTED_EDGE('',*,*,#3156,.F.);
#4564=PLANE('',#5817);
#4565=PLANE('',#5818);
#4566=PLANE('',#5819);
#4567=PLANE('',#5820);
#4568=PLANE('',#5821);
#4569=PLANE('',#5822);
#4570=PLANE('',#5823);
#4571=PLANE('',#5824);
#4572=PLANE('',#5825);
#4573=PLANE('',#5827);
#4574=PLANE('',#5835);
#4836=ADVANCED_FACE('',(#1460),#4564,.F.);
#4837=ADVANCED_FACE('',(#1461),#4565,.F.);
#4838=ADVANCED_FACE('',(#1462),#4566,.F.);
#4839=ADVANCED_FACE('',(#1463),#4567,.F.);
#4840=ADVANCED_FACE('',(#1464),#4568,.F.);
#4841=ADVANCED_FACE('',(#1465),#4569,.F.);
#4842=ADVANCED_FACE('',(#1466),#4570,.F.);
#4843=ADVANCED_FACE('',(#1467),#4571,.F.);
#4844=ADVANCED_FACE('',(#1468),#4572,.F.);
#4845=ADVANCED_FACE('',(#1469),#4573,.T.);
#4846=ADVANCED_FACE('',(#1470),#282,.T.);
#4847=ADVANCED_FACE('',(#1471),#1093,.T.);
#4848=ADVANCED_FACE('',(#1472),#283,.T.);
#4849=ADVANCED_FACE('',(#1473,#1211),#4574,.T.);
#4850=ADVANCED_FACE('',(#1474),#284,.T.);
#4851=ADVANCED_FACE('',(#1475),#1094,.T.);
#4922=CLOSED_SHELL('',(#4836,#4837,#4838,#4839,#4840,#4841,#4842,#4843));
#4923=CLOSED_SHELL('',(#4844,#4845,#4846,#4847,#4848,#4849,#4850,#4851));
#5816=AXIS2_PLACEMENT_3D('',#9068,#7261,#7262);
#5817=AXIS2_PLACEMENT_3D('',#9069,#7263,#7264);
#5818=AXIS2_PLACEMENT_3D('',#9078,#7269,#7270);
#5819=AXIS2_PLACEMENT_3D('',#9084,#7274,#7275);
#5820=AXIS2_PLACEMENT_3D('',#9090,#7279,#7280);
#5821=AXIS2_PLACEMENT_3D('',#9096,#7284,#7285);
#5822=AXIS2_PLACEMENT_3D('',#9102,#7289,#7290);
#5823=AXIS2_PLACEMENT_3D('',#9105,#7293,#7294);
#5824=AXIS2_PLACEMENT_3D('',#9106,#7295,#7296);
#5825=AXIS2_PLACEMENT_3D('',#9107,#7297,#7298);
#5826=AXIS2_PLACEMENT_3D('',#9109,#7299,#7300);
#5827=AXIS2_PLACEMENT_3D('',#9110,#7301,#7302);
#5828=AXIS2_PLACEMENT_3D('',#9112,#7303,#7304);
#5829=AXIS2_PLACEMENT_3D('',#9113,#7305,#7306);
#5830=AXIS2_PLACEMENT_3D('',#9115,#7307,#7308);
#5831=AXIS2_PLACEMENT_3D('',#9117,#7310,#7311);
#5832=AXIS2_PLACEMENT_3D('',#9119,#7312,#7313);
#5833=AXIS2_PLACEMENT_3D('',#9121,#7315,#7316);
#5834=AXIS2_PLACEMENT_3D('',#9123,#7317,#7318);
#5835=AXIS2_PLACEMENT_3D('',#9125,#7320,#7321);
#5836=AXIS2_PLACEMENT_3D('',#9127,#7322,#7323);
#5837=AXIS2_PLACEMENT_3D('',#9128,#7324,#7325);
#5838=AXIS2_PLACEMENT_3D('',#9130,#7326,#7327);
#5839=AXIS2_PLACEMENT_3D('',#9132,#7329,#7330);
#7261=DIRECTION('axis',(0.,0.,1.));
#7262=DIRECTION('refdir',(1.,0.,0.));
#7263=DIRECTION('center_axis',(0.866025403784439,0.,-0.5));
#7264=DIRECTION('ref_axis',(0.5,0.,0.866025403784439));
#7265=DIRECTION('',(-0.5,0.,-0.866025403784439));
#7266=DIRECTION('',(0.,-1.,0.));
#7267=DIRECTION('',(0.5,0.,0.866025403784439));
#7268=DIRECTION('',(0.,-1.,0.));
#7269=DIRECTION('center_axis',(1.60246890531964E-16,0.,-1.));
#7270=DIRECTION('ref_axis',(1.,0.,1.60246890531964E-16));
#7271=DIRECTION('',(-1.,0.,-1.60246890531964E-16));
#7272=DIRECTION('',(0.,-1.,0.));
#7273=DIRECTION('',(1.,0.,1.60246890531964E-16));
#7274=DIRECTION('center_axis',(-0.866025403784439,0.,-0.5));
#7275=DIRECTION('ref_axis',(0.5,0.,-0.866025403784439));
#7276=DIRECTION('',(-0.5,0.,0.866025403784439));
#7277=DIRECTION('',(0.,-1.,0.));
#7278=DIRECTION('',(0.5,0.,-0.866025403784439));
#7279=DIRECTION('center_axis',(-0.866025403784439,0.,0.5));
#7280=DIRECTION('ref_axis',(-0.5,0.,-0.866025403784439));
#7281=DIRECTION('',(0.5,0.,0.866025403784439));
#7282=DIRECTION('',(0.,-1.,0.));
#7283=DIRECTION('',(-0.5,0.,-0.866025403784439));
#7284=DIRECTION('center_axis',(-1.60246890531964E-16,0.,1.));
#7285=DIRECTION('ref_axis',(-1.,0.,-1.60246890531964E-16));
#7286=DIRECTION('',(1.,0.,1.60246890531964E-16));
#7287=DIRECTION('',(0.,-1.,0.));
#7288=DIRECTION('',(-1.,0.,-1.60246890531964E-16));
#7289=DIRECTION('center_axis',(0.866025403784439,0.,0.5));
#7290=DIRECTION('ref_axis',(-0.5,0.,0.866025403784439));
#7291=DIRECTION('',(0.5,0.,-0.866025403784439));
#7292=DIRECTION('',(-0.5,0.,0.866025403784439));
#7293=DIRECTION('center_axis',(0.,1.,0.));
#7294=DIRECTION('ref_axis',(1.,0.,0.));
#7295=DIRECTION('center_axis',(0.,-1.,0.));
#7296=DIRECTION('ref_axis',(0.,0.,-1.));
#7297=DIRECTION('center_axis',(0.,1.,0.));
#7298=DIRECTION('ref_axis',(1.,0.,0.));
#7299=DIRECTION('center_axis',(0.,1.,0.));
#7300=DIRECTION('ref_axis',(1.,0.,0.));
#7301=DIRECTION('center_axis',(0.,1.,0.));
#7302=DIRECTION('ref_axis',(0.,0.,1.));
#7303=DIRECTION('center_axis',(0.,-1.,0.));
#7304=DIRECTION('ref_axis',(1.,0.,0.));
#7305=DIRECTION('center_axis',(0.,-1.,0.));
#7306=DIRECTION('ref_axis',(1.,0.,0.));
#7307=DIRECTION('center_axis',(0.,-1.,0.));
#7308=DIRECTION('ref_axis',(1.,0.,0.));
#7309=DIRECTION('',(0.707106781186547,0.707106781186548,8.65956056235493E-17));
#7310=DIRECTION('center_axis',(0.,-1.,0.));
#7311=DIRECTION('ref_axis',(1.,0.,0.));
#7312=DIRECTION('center_axis',(0.,-1.,0.));
#7313=DIRECTION('ref_axis',(1.,0.,0.));
#7314=DIRECTION('',(0.,1.,0.));
#7315=DIRECTION('center_axis',(0.,1.,0.));
#7316=DIRECTION('ref_axis',(1.,0.,0.));
#7317=DIRECTION('center_axis',(0.,-1.,0.));
#7318=DIRECTION('ref_axis',(1.,0.,0.));
#7319=DIRECTION('',(-0.707106781186547,0.707106781186548,-8.65956056235493E-17));
#7320=DIRECTION('center_axis',(0.,-1.,0.));
#7321=DIRECTION('ref_axis',(0.,0.,-1.));
#7322=DIRECTION('center_axis',(0.,-1.,0.));
#7323=DIRECTION('ref_axis',(1.,0.,0.));
#7324=DIRECTION('center_axis',(0.,1.,0.));
#7325=DIRECTION('ref_axis',(1.,0.,0.));
#7326=DIRECTION('center_axis',(0.,1.,0.));
#7327=DIRECTION('ref_axis',(1.,0.,0.));
#7328=DIRECTION('',(-0.447213595499958,0.894427190999916,-5.47678698264203E-17));
#7329=DIRECTION('center_axis',(0.,-1.,0.));
#7330=DIRECTION('ref_axis',(1.,0.,0.));
#7331=DIRECTION('',(0.,1.,0.));
#9068=CARTESIAN_POINT('',(0.,0.,0.));
#9069=CARTESIAN_POINT('Origin',(0.0866025403784439,-0.4,-0.15));
#9070=CARTESIAN_POINT('',(0.173205080756888,-0.4,0.));
#9071=CARTESIAN_POINT('',(0.0866025403784439,-0.4,-0.15));
#9072=CARTESIAN_POINT('',(0.173205080756888,-0.4,0.));
#9073=CARTESIAN_POINT('',(0.0866025403784439,-0.64,-0.15));
#9074=CARTESIAN_POINT('',(0.0866025403784439,-0.4,-0.15));
#9075=CARTESIAN_POINT('',(0.173205080756888,-0.64,0.));
#9076=CARTESIAN_POINT('',(0.173205080756888,-0.64,0.));
#9077=CARTESIAN_POINT('',(0.173205080756888,-0.4,0.));
#9078=CARTESIAN_POINT('Origin',(-0.0866025403784438,-0.4,-0.15));
#9079=CARTESIAN_POINT('',(-0.0866025403784438,-0.4,-0.15));
#9080=CARTESIAN_POINT('',(0.0866025403784439,-0.4,-0.15));
#9081=CARTESIAN_POINT('',(-0.0866025403784438,-0.64,-0.15));
#9082=CARTESIAN_POINT('',(-0.0866025403784438,-0.4,-0.15));
#9083=CARTESIAN_POINT('',(0.0866025403784439,-0.64,-0.15));
#9084=CARTESIAN_POINT('Origin',(-0.173205080756888,-0.4,-2.77555756156289E-17));
#9085=CARTESIAN_POINT('',(-0.173205080756888,-0.4,-2.12115047744981E-17));
#9086=CARTESIAN_POINT('',(-0.0866025403784438,-0.4,-0.15));
#9087=CARTESIAN_POINT('',(-0.173205080756888,-0.64,-2.77555756156289E-17));
#9088=CARTESIAN_POINT('',(-0.173205080756888,-0.4,-2.12115047744981E-17));
#9089=CARTESIAN_POINT('',(-0.0866025403784438,-0.64,-0.15));
#9090=CARTESIAN_POINT('Origin',(-0.0866025403784439,-0.4,0.15));
#9091=CARTESIAN_POINT('',(-0.0866025403784439,-0.4,0.15));
#9092=CARTESIAN_POINT('',(-0.173205080756888,-0.4,-2.12115047744981E-17));
#9093=CARTESIAN_POINT('',(-0.0866025403784439,-0.64,0.15));
#9094=CARTESIAN_POINT('',(-0.0866025403784439,-0.4,0.15));
#9095=CARTESIAN_POINT('',(-0.173205080756888,-0.64,-2.12115047744981E-17));
#9096=CARTESIAN_POINT('Origin',(0.0866025403784439,-0.4,0.15));
#9097=CARTESIAN_POINT('',(0.0866025403784439,-0.4,0.15));
#9098=CARTESIAN_POINT('',(-0.0866025403784439,-0.4,0.15));
#9099=CARTESIAN_POINT('',(0.0866025403784439,-0.64,0.15));
#9100=CARTESIAN_POINT('',(0.0866025403784439,-0.4,0.15));
#9101=CARTESIAN_POINT('',(-0.0866025403784439,-0.64,0.15));
#9102=CARTESIAN_POINT('Origin',(0.173205080756888,-0.4,0.));
#9103=CARTESIAN_POINT('',(0.0866025403784439,-0.4,0.15));
#9104=CARTESIAN_POINT('',(0.0866025403784439,-0.64,0.15));
#9105=CARTESIAN_POINT('Origin',(0.,-0.4,-2.77555756156289E-17));
#9106=CARTESIAN_POINT('Origin',(0.,-0.64,-2.77555756156289E-17));
#9107=CARTESIAN_POINT('Origin',(0.,-1.,0.));
#9108=CARTESIAN_POINT('',(-0.1954,-1.,2.39295984553393E-17));
#9109=CARTESIAN_POINT('Origin',(0.,-1.,0.));
#9110=CARTESIAN_POINT('Origin',(0.3,0.4,0.));
#9111=CARTESIAN_POINT('',(-0.3,0.4,-3.67394039744206E-17));
#9112=CARTESIAN_POINT('Origin',(0.,0.4,0.));
#9113=CARTESIAN_POINT('Origin',(0.,0.375,0.));
#9114=CARTESIAN_POINT('',(-0.35,0.35,-4.28626379701573E-17));
#9115=CARTESIAN_POINT('Origin',(0.,0.35,0.));
#9116=CARTESIAN_POINT('',(-0.325,0.375,-3.9801020972289E-17));
#9117=CARTESIAN_POINT('Origin',(0.,0.19,0.));
#9118=CARTESIAN_POINT('',(-0.35,0.03,-4.28626379701574E-17));
#9119=CARTESIAN_POINT('Origin',(0.,0.03,0.));
#9120=CARTESIAN_POINT('',(-0.35,0.19,-4.28626379701574E-17));
#9121=CARTESIAN_POINT('Origin',(0.,0.0149999999999999,0.));
#9122=CARTESIAN_POINT('',(-0.32,-3.29597460435593E-17,-3.91886975727153E-17));
#9123=CARTESIAN_POINT('Origin',(0.,0.,0.));
#9124=CARTESIAN_POINT('',(-0.335,0.0149999999999999,-4.10256677714363E-17));
#9125=CARTESIAN_POINT('Origin',(0.22,0.,0.));
#9126=CARTESIAN_POINT('',(-0.22,-6.93889390390723E-18,-2.69422295812418E-17));
#9127=CARTESIAN_POINT('Origin',(0.,0.,0.));
#9128=CARTESIAN_POINT('Origin',(0.,-0.02,0.));
#9129=CARTESIAN_POINT('',(-0.1954,-0.0492,2.39295984553393E-17));
#9130=CARTESIAN_POINT('Origin',(0.,-0.0492,0.));
#9131=CARTESIAN_POINT('',(-0.21,-0.02,-2.57175827820944E-17));
#9132=CARTESIAN_POINT('Origin',(0.,-0.8,0.));
#9133=CARTESIAN_POINT('',(-0.1954,-0.8,-2.39295984553393E-17));
#9347=UNCERTAINTY_MEASURE_WITH_UNIT(LENGTH_MEASURE(0.001),#9392,
'DISTANCE_ACCURACY_VALUE',
'Maximum model space distance between geometric entities at asserted c
onnectivities');
#9354=UNCERTAINTY_MEASURE_WITH_UNIT(LENGTH_MEASURE(0.001),#9392,
'DISTANCE_ACCURACY_VALUE',
'Maximum model space distance between geometric entities at asserted c
onnectivities');
#9384=(
GEOMETRIC_REPRESENTATION_CONTEXT(3)
GLOBAL_UNCERTAINTY_ASSIGNED_CONTEXT((#9347))
GLOBAL_UNIT_ASSIGNED_CONTEXT((#9392,#9394,#9395))
REPRESENTATION_CONTEXT('','3D')
);
#9391=(
GEOMETRIC_REPRESENTATION_CONTEXT(3)
GLOBAL_UNCERTAINTY_ASSIGNED_CONTEXT((#9354))
GLOBAL_UNIT_ASSIGNED_CONTEXT((#9392,#9394,#9395))
REPRESENTATION_CONTEXT('','3D')
);
#9392=(
LENGTH_UNIT()
NAMED_UNIT(*)
SI_UNIT(.CENTI.,.METRE.)
);
#9394=(
NAMED_UNIT(*)
PLANE_ANGLE_UNIT()
SI_UNIT($,.RADIAN.)
);
#9395=(
NAMED_UNIT(*)
SI_UNIT($,.STERADIAN.)
SOLID_ANGLE_UNIT()
);
#9425=SHAPE_DEFINITION_REPRESENTATION(#9491,#9549);
#9491=PRODUCT_DEFINITION_SHAPE('',$,#9586);
#9549=SHAPE_REPRESENTATION('',(#5816),#9384);
#9556=PRODUCT_DEFINITION_CONTEXT('part definition',#9666,'design');
#9586=PRODUCT_DEFINITION('M4x10 Cap Screw','M4x10 Cap Screw',#9622,#9556);
#9622=PRODUCT_DEFINITION_FORMATION('',$,#9697);
#9666=APPLICATION_CONTEXT(
'Core Data for Automotive Mechanical Design Process');
#9667=PRODUCT_CONTEXT('part definition',#9666,'mechanical');
#9697=PRODUCT('M4x10 Cap Screw','M4x10 Cap Screw','M4x10 Cap Screw',(#9667));
#9760=COLOUR_RGB('Black',0.12,0.14,0.17);
#9761=FILL_AREA_STYLE_COLOUR('',#9760);
#9762=FILL_AREA_STYLE('',(#9761));
#9763=SURFACE_STYLE_FILL_AREA(#9762);
#9764=SURFACE_SIDE_STYLE('',(#9763));
#9765=SURFACE_STYLE_USAGE(.BOTH.,#9764);
#9766=PRESENTATION_STYLE_ASSIGNMENT((#9765));
ENDSEC;
END-ISO-10303-21;
